ISO-10303-21;
HEADER;
/* Generated by software containing ST-Developer
 * from STEP Tools, Inc. (www.steptools.com) 
 */

FILE_DESCRIPTION(
/* description */ ('Air blow-off nozzle station'),
/* implementation_level */ '2;1');

FILE_NAME(
/* name */ 'Cap Screw - M4x16.step',
/* time_stamp */ '2026-10-27T10:53:54-07:00',
/* author */ (''),
/* organization */ (''),
/* preprocessor_version */ 'ST-DEVELOPER v20.2',
/* originating_system */ 'Autodesk Translation Framework v15.17.0.0',
/* authorisation */ '');

FILE_SCHEMA (('AUTOMOTIVE_DESIGN { 1 0 10303 214 3 1 1 }'));
ENDSEC;

DATA;
#10=MECHANICAL_DESIGN_GEOMETRIC_PRESENTATION_REPRESENTATION('',(#249),#7897);
#152=ORIENTED_CLOSED_SHELL('',*,#4300,.F.);
#154=BREP_WITH_VOIDS('Body1',#4299,(#152));
#159=CONICAL_SURFACE('',#4837,0.325,0.785398163397448);
#160=CONICAL_SURFACE('',#4841,0.335,0.785398163397448);
#161=CONICAL_SURFACE('',#4845,0.21,0.463647609000806);
#162=CONICAL_SURFACE('',#4849,0.18,0.785398163397448);
#199=SHAPE_REPRESENTATION_RELATIONSHIP('SRR','None',#8013,#224);
#224=ADVANCED_BREP_SHAPE_REPRESENTATION('',(#154),#7880);
#249=STYLED_ITEM('',(#8227),#154);
#330=FACE_BOUND('',#999,.T.);
#483=PLANE('',#4835);
#484=PLANE('',#4843);
#485=PLANE('',#4851);
#486=PLANE('',#4852);
#487=PLANE('',#4853);
#488=PLANE('',#4854);
#489=PLANE('',#4855);
#490=PLANE('',#4856);
#491=PLANE('',#4857);
#492=PLANE('',#4858);
#493=PLANE('',#4859);
#693=FACE_OUTER_BOUND('',#994,.T.);
#694=FACE_OUTER_BOUND('',#995,.T.);
#695=FACE_OUTER_BOUND('',#996,.T.);
#696=FACE_OUTER_BOUND('',#997,.T.);
#697=FACE_OUTER_BOUND('',#998,.T.);
#698=FACE_OUTER_BOUND('',#1000,.T.);
#699=FACE_OUTER_BOUND('',#1001,.T.);
#700=FACE_OUTER_BOUND('',#1002,.T.);
#701=FACE_OUTER_BOUND('',#1003,.T.);
#702=FACE_OUTER_BOUND('',#1004,.T.);
#703=FACE_OUTER_BOUND('',#1005,.T.);
#704=FACE_OUTER_BOUND('',#1006,.T.);
#705=FACE_OUTER_BOUND('',#1007,.T.);
#706=FACE_OUTER_BOUND('',#1008,.T.);
#707=FACE_OUTER_BOUND('',#1009,.T.);
#708=FACE_OUTER_BOUND('',#1010,.T.);
#709=FACE_OUTER_BOUND('',#1011,.T.);
#994=EDGE_LOOP('',(#3599));
#995=EDGE_LOOP('',(#3600,#3601,#3602,#3603));
#996=EDGE_LOOP('',(#3604,#3605,#3606,#3607));
#997=EDGE_LOOP('',(#3608,#3609,#3610,#3611));
#998=EDGE_LOOP('',(#3612));
#999=EDGE_LOOP('',(#3613));
#1000=EDGE_LOOP('',(#3614,#3615,#3616,#3617));
#1001=EDGE_LOOP('',(#3618,#3619,#3620,#3621));
#1002=EDGE_LOOP('',(#3622,#3623,#3624,#3625));
#1003=EDGE_LOOP('',(#3626));
#1004=EDGE_LOOP('',(#3627,#3628,#3629,#3630));
#1005=EDGE_LOOP('',(#3631,#3632,#3633,#3634));
#1006=EDGE_LOOP('',(#3635,#3636,#3637,#3638));
#1007=EDGE_LOOP('',(#3639,#3640,#3641,#3642));
#1008=EDGE_LOOP('',(#3643,#3644,#3645,#3646));
#1009=EDGE_LOOP('',(#3647,#3648,#3649,#3650));
#1010=EDGE_LOOP('',(#3651,#3652,#3653,#3654,#3655,#3656));
#1011=EDGE_LOOP('',(#3657,#3658,#3659,#3660,#3661,#3662));
#1395=LINE('',#7384,#1749);
#1396=LINE('',#7388,#1750);
#1397=LINE('',#7392,#1751);
#1398=LINE('',#7399,#1752);
#1399=LINE('',#7403,#1753);
#1400=LINE('',#7407,#1754);
#1401=LINE('',#7412,#1755);
#1402=LINE('',#7414,#1756);
#1403=LINE('',#7416,#1757);
#1404=LINE('',#7417,#1758);
#1405=LINE('',#7420,#1759);
#1406=LINE('',#7422,#1760);
#1407=LINE('',#7423,#1761);
#1408=LINE('',#7426,#1762);
#1409=LINE('',#7428,#1763);
#1410=LINE('',#7429,#1764);
#1411=LINE('',#7432,#1765);
#1412=LINE('',#7434,#1766);
#1413=LINE('',#7435,#1767);
#1414=LINE('',#7438,#1768);
#1415=LINE('',#7440,#1769);
#1416=LINE('',#7441,#1770);
#1417=LINE('',#7443,#1771);
#1418=LINE('',#7444,#1772);
#1749=VECTOR('',#5829,0.325);
#1750=VECTOR('',#5834,0.35);
#1751=VECTOR('',#5839,0.335);
#1752=VECTOR('',#5848,0.21);
#1753=VECTOR('',#5853,0.2);
#1754=VECTOR('',#5858,0.18);
#1755=VECTOR('',#5863,1.);
#1756=VECTOR('',#5864,1.);
#1757=VECTOR('',#5865,1.);
#1758=VECTOR('',#5866,1.);
#1759=VECTOR('',#5869,1.);
#1760=VECTOR('',#5870,1.);
#1761=VECTOR('',#5871,1.);
#1762=VECTOR('',#5874,1.);
#1763=VECTOR('',#5875,1.);
#1764=VECTOR('',#5876,1.);
#1765=VECTOR('',#5879,1.);
#1766=VECTOR('',#5880,1.);
#1767=VECTOR('',#5881,1.);
#1768=VECTOR('',#5884,1.);
#1769=VECTOR('',#5885,1.);
#1770=VECTOR('',#5886,1.);
#1771=VECTOR('',#5889,1.);
#1772=VECTOR('',#5890,1.);
#1924=CIRCLE('',#4836,0.3);
#1925=CIRCLE('',#4838,0.35);
#1926=CIRCLE('',#4840,0.35);
#1927=CIRCLE('',#4842,0.32);
#1928=CIRCLE('',#4844,0.22);
#1929=CIRCLE('',#4846,0.1954);
#1930=CIRCLE('',#4848,0.1954);
#1931=CIRCLE('',#4850,0.16);
#2244=VERTEX_POINT('',#7379);
#2245=VERTEX_POINT('',#7382);
#2246=VERTEX_POINT('',#7386);
#2247=VERTEX_POINT('',#7390);
#2248=VERTEX_POINT('',#7394);
#2249=VERTEX_POINT('',#7397);
#2250=VERTEX_POINT('',#7401);
#2251=VERTEX_POINT('',#7405);
#2252=VERTEX_POINT('',#7410);
#2253=VERTEX_POINT('',#7411);
#2254=VERTEX_POINT('',#7413);
#2255=VERTEX_POINT('',#7415);
#2256=VERTEX_POINT('',#7419);
#2257=VERTEX_POINT('',#7421);
#2258=VERTEX_POINT('',#7425);
#2259=VERTEX_POINT('',#7427);
#2260=VERTEX_POINT('',#7431);
#2261=VERTEX_POINT('',#7433);
#2262=VERTEX_POINT('',#7437);
#2263=VERTEX_POINT('',#7439);
#2717=EDGE_CURVE('',#2244,#2244,#1924,.T.);
#2718=EDGE_CURVE('',#2245,#2245,#1925,.T.);
#2719=EDGE_CURVE('',#2245,#2244,#1395,.T.);
#2720=EDGE_CURVE('',#2246,#2246,#1926,.T.);
#2721=EDGE_CURVE('',#2246,#2245,#1396,.T.);
#2722=EDGE_CURVE('',#2247,#2247,#1927,.T.);
#2723=EDGE_CURVE('',#2247,#2246,#1397,.T.);
#2724=EDGE_CURVE('',#2248,#2248,#1928,.T.);
#2725=EDGE_CURVE('',#2249,#2249,#1929,.F.);
#2726=EDGE_CURVE('',#2249,#2248,#1398,.T.);
#2727=EDGE_CURVE('',#2250,#2250,#1930,.F.);
#2728=EDGE_CURVE('',#2250,#2249,#1399,.T.);
#2729=EDGE_CURVE('',#2251,#2251,#1931,.T.);
#2730=EDGE_CURVE('',#2251,#2250,#1400,.T.);
#2731=EDGE_CURVE('',#2252,#2253,#1401,.T.);
#2732=EDGE_CURVE('',#2253,#2254,#1402,.T.);
#2733=EDGE_CURVE('',#2254,#2255,#1403,.T.);
#2734=EDGE_CURVE('',#2252,#2255,#1404,.T.);
#2735=EDGE_CURVE('',#2253,#2256,#1405,.T.);
#2736=EDGE_CURVE('',#2256,#2257,#1406,.T.);
#2737=EDGE_CURVE('',#2257,#2254,#1407,.T.);
#2738=EDGE_CURVE('',#2256,#2258,#1408,.T.);
#2739=EDGE_CURVE('',#2258,#2259,#1409,.T.);
#2740=EDGE_CURVE('',#2259,#2257,#1410,.T.);
#2741=EDGE_CURVE('',#2258,#2260,#1411,.T.);
#2742=EDGE_CURVE('',#2260,#2261,#1412,.T.);
#2743=EDGE_CURVE('',#2261,#2259,#1413,.T.);
#2744=EDGE_CURVE('',#2260,#2262,#1414,.T.);
#2745=EDGE_CURVE('',#2262,#2263,#1415,.T.);
#2746=EDGE_CURVE('',#2263,#2261,#1416,.T.);
#2747=EDGE_CURVE('',#2262,#2252,#1417,.T.);
#2748=EDGE_CURVE('',#2255,#2263,#1418,.T.);
#3599=ORIENTED_EDGE('',*,*,#2717,.F.);
#3600=ORIENTED_EDGE('',*,*,#2718,.F.);
#3601=ORIENTED_EDGE('',*,*,#2719,.T.);
#3602=ORIENTED_EDGE('',*,*,#2717,.T.);
#3603=ORIENTED_EDGE('',*,*,#2719,.F.);
#3604=ORIENTED_EDGE('',*,*,#2720,.F.);
#3605=ORIENTED_EDGE('',*,*,#2721,.T.);
#3606=ORIENTED_EDGE('',*,*,#2718,.T.);
#3607=ORIENTED_EDGE('',*,*,#2721,.F.);
#3608=ORIENTED_EDGE('',*,*,#2722,.F.);
#3609=ORIENTED_EDGE('',*,*,#2723,.T.);
#3610=ORIENTED_EDGE('',*,*,#2720,.T.);
#3611=ORIENTED_EDGE('',*,*,#2723,.F.);
#3612=ORIENTED_EDGE('',*,*,#2722,.T.);
#3613=ORIENTED_EDGE('',*,*,#2724,.F.);
#3614=ORIENTED_EDGE('',*,*,#2725,.F.);
#3615=ORIENTED_EDGE('',*,*,#2726,.T.);
#3616=ORIENTED_EDGE('',*,*,#2724,.T.);
#3617=ORIENTED_EDGE('',*,*,#2726,.F.);
#3618=ORIENTED_EDGE('',*,*,#2727,.F.);
#3619=ORIENTED_EDGE('',*,*,#2728,.T.);
#3620=ORIENTED_EDGE('',*,*,#2725,.T.);
#3621=ORIENTED_EDGE('',*,*,#2728,.F.);
#3622=ORIENTED_EDGE('',*,*,#2729,.F.);
#3623=ORIENTED_EDGE('',*,*,#2730,.T.);
#3624=ORIENTED_EDGE('',*,*,#2727,.T.);
#3625=ORIENTED_EDGE('',*,*,#2730,.F.);
#3626=ORIENTED_EDGE('',*,*,#2729,.T.);
#3627=ORIENTED_EDGE('',*,*,#2731,.T.);
#3628=ORIENTED_EDGE('',*,*,#2732,.T.);
#3629=ORIENTED_EDGE('',*,*,#2733,.T.);
#3630=ORIENTED_EDGE('',*,*,#2734,.F.);
#3631=ORIENTED_EDGE('',*,*,#2735,.T.);
#3632=ORIENTED_EDGE('',*,*,#2736,.T.);
#3633=ORIENTED_EDGE('',*,*,#2737,.T.);
#3634=ORIENTED_EDGE('',*,*,#2732,.F.);
#3635=ORIENTED_EDGE('',*,*,#2738,.T.);
#3636=ORIENTED_EDGE('',*,*,#2739,.T.);
#3637=ORIENTED_EDGE('',*,*,#2740,.T.);
#3638=ORIENTED_EDGE('',*,*,#2736,.F.);
#3639=ORIENTED_EDGE('',*,*,#2741,.T.);
#3640=ORIENTED_EDGE('',*,*,#2742,.T.);
#3641=ORIENTED_EDGE('',*,*,#2743,.T.);
#3642=ORIENTED_EDGE('',*,*,#2739,.F.);
#3643=ORIENTED_EDGE('',*,*,#2744,.T.);
#3644=ORIENTED_EDGE('',*,*,#2745,.T.);
#3645=ORIENTED_EDGE('',*,*,#2746,.T.);
#3646=ORIENTED_EDGE('',*,*,#2742,.F.);
#3647=ORIENTED_EDGE('',*,*,#2747,.T.);
#3648=ORIENTED_EDGE('',*,*,#2734,.T.);
#3649=ORIENTED_EDGE('',*,*,#2748,.T.);
#3650=ORIENTED_EDGE('',*,*,#2745,.F.);
#3651=ORIENTED_EDGE('',*,*,#2747,.F.);
#3652=ORIENTED_EDGE('',*,*,#2744,.F.);
#3653=ORIENTED_EDGE('',*,*,#2741,.F.);
#3654=ORIENTED_EDGE('',*,*,#2738,.F.);
#3655=ORIENTED_EDGE('',*,*,#2735,.F.);
#3656=ORIENTED_EDGE('',*,*,#2731,.F.);
#3657=ORIENTED_EDGE('',*,*,#2748,.F.);
#3658=ORIENTED_EDGE('',*,*,#2733,.F.);
#3659=ORIENTED_EDGE('',*,*,#2737,.F.);
#3660=ORIENTED_EDGE('',*,*,#2740,.F.);
#3661=ORIENTED_EDGE('',*,*,#2743,.F.);
#3662=ORIENTED_EDGE('',*,*,#2746,.F.);
#3993=CYLINDRICAL_SURFACE('',#4839,0.35);
#3994=CYLINDRICAL_SURFACE('',#4847,0.1954);
#4183=ADVANCED_FACE('',(#693),#483,.T.);
#4184=ADVANCED_FACE('',(#694),#159,.T.);
#4185=ADVANCED_FACE('',(#695),#3993,.T.);
#4186=ADVANCED_FACE('',(#696),#160,.T.);
#4187=ADVANCED_FACE('',(#697,#330),#484,.T.);
#4188=ADVANCED_FACE('',(#698),#161,.T.);
#4189=ADVANCED_FACE('',(#699),#3994,.T.);
#4190=ADVANCED_FACE('',(#700),#162,.T.);
#4191=ADVANCED_FACE('',(#701),#485,.T.);
#4192=ADVANCED_FACE('',(#702),#486,.F.);
#4193=ADVANCED_FACE('',(#703),#487,.F.);
#4194=ADVANCED_FACE('',(#704),#488,.F.);
#4195=ADVANCED_FACE('',(#705),#489,.F.);
#4196=ADVANCED_FACE('',(#706),#490,.F.);
#4197=ADVANCED_FACE('',(#707),#491,.F.);
#4198=ADVANCED_FACE('',(#708),#492,.F.);
#4199=ADVANCED_FACE('',(#709),#493,.F.);
#4299=CLOSED_SHELL('',(#4183,#4184,#4185,#4186,#4187,#4188,#4189,#4190,
#4191));
#4300=CLOSED_SHELL('',(#4192,#4193,#4194,#4195,#4196,#4197,#4198,#4199));
#4834=AXIS2_PLACEMENT_3D('',#7377,#5819,#5820);
#4835=AXIS2_PLACEMENT_3D('',#7378,#5821,#5822);
#4836=AXIS2_PLACEMENT_3D('',#7380,#5823,#5824);
#4837=AXIS2_PLACEMENT_3D('',#7381,#5825,#5826);
#4838=AXIS2_PLACEMENT_3D('',#7383,#5827,#5828);
#4839=AXIS2_PLACEMENT_3D('',#7385,#5830,#5831);
#4840=AXIS2_PLACEMENT_3D('',#7387,#5832,#5833);
#4841=AXIS2_PLACEMENT_3D('',#7389,#5835,#5836);
#4842=AXIS2_PLACEMENT_3D('',#7391,#5837,#5838);
#4843=AXIS2_PLACEMENT_3D('',#7393,#5840,#5841);
#4844=AXIS2_PLACEMENT_3D('',#7395,#5842,#5843);
#4845=AXIS2_PLACEMENT_3D('',#7396,#5844,#5845);
#4846=AXIS2_PLACEMENT_3D('',#7398,#5846,#5847);
#4847=AXIS2_PLACEMENT_3D('',#7400,#5849,#5850);
#4848=AXIS2_PLACEMENT_3D('',#7402,#5851,#5852);
#4849=AXIS2_PLACEMENT_3D('',#7404,#5854,#5855);
#4850=AXIS2_PLACEMENT_3D('',#7406,#5856,#5857);
#4851=AXIS2_PLACEMENT_3D('',#7408,#5859,#5860);
#4852=AXIS2_PLACEMENT_3D('',#7409,#5861,#5862);
#4853=AXIS2_PLACEMENT_3D('',#7418,#5867,#5868);
#4854=AXIS2_PLACEMENT_3D('',#7424,#5872,#5873);
#4855=AXIS2_PLACEMENT_3D('',#7430,#5877,#5878);
#4856=AXIS2_PLACEMENT_3D('',#7436,#5882,#5883);
#4857=AXIS2_PLACEMENT_3D('',#7442,#5887,#5888);
#4858=AXIS2_PLACEMENT_3D('',#7445,#5891,#5892);
#4859=AXIS2_PLACEMENT_3D('',#7446,#5893,#5894);
#5819=DIRECTION('axis',(0.,0.,1.));
#5820=DIRECTION('refdir',(1.,0.,0.));
#5821=DIRECTION('center_axis',(0.,1.,0.));
#5822=DIRECTION('ref_axis',(0.,0.,1.));
#5823=DIRECTION('center_axis',(0.,-1.,0.));
#5824=DIRECTION('ref_axis',(1.,0.,0.));
#5825=DIRECTION('center_axis',(0.,-1.,0.));
#5826=DIRECTION('ref_axis',(1.,0.,0.));
#5827=DIRECTION('center_axis',(0.,-1.,0.));
#5828=DIRECTION('ref_axis',(1.,0.,0.));
#5829=DIRECTION('',(0.707106781186547,0.707106781186548,8.65956056235493E-17));
#5830=DIRECTION('center_axis',(0.,-1.,0.));
#5831=DIRECTION('ref_axis',(1.,0.,0.));
#5832=DIRECTION('center_axis',(0.,-1.,0.));
#5833=DIRECTION('ref_axis',(1.,0.,0.));
#5834=DIRECTION('',(0.,1.,0.));
#5835=DIRECTION('center_axis',(0.,1.,0.));
#5836=DIRECTION('ref_axis',(1.,0.,0.));
#5837=DIRECTION('center_axis',(0.,-1.,0.));
#5838=DIRECTION('ref_axis',(1.,0.,0.));
#5839=DIRECTION('',(-0.707106781186547,0.707106781186548,-8.65956056235493E-17));
#5840=DIRECTION('center_axis',(0.,-1.,0.));
#5841=DIRECTION('ref_axis',(0.,0.,-1.));
#5842=DIRECTION('center_axis',(0.,-1.,0.));
#5843=DIRECTION('ref_axis',(1.,0.,0.));
#5844=DIRECTION('center_axis',(0.,1.,0.));
#5845=DIRECTION('ref_axis',(1.,0.,0.));
#5846=DIRECTION('center_axis',(0.,1.,0.));
#5847=DIRECTION('ref_axis',(1.,0.,0.));
#5848=DIRECTION('',(-0.447213595499958,0.894427190999916,-5.47678698264203E-17));
#5849=DIRECTION('center_axis',(0.,-1.,0.));
#5850=DIRECTION('ref_axis',(1.,0.,0.));
#5851=DIRECTION('center_axis',(0.,1.,0.));
#5852=DIRECTION('ref_axis',(1.,0.,0.));
#5853=DIRECTION('',(0.,1.,0.));
#5854=DIRECTION('center_axis',(0.,1.,0.));
#5855=DIRECTION('ref_axis',(1.,0.,0.));
#5856=DIRECTION('center_axis',(0.,-1.,0.));
#5857=DIRECTION('ref_axis',(1.,0.,0.));
#5858=DIRECTION('',(-0.707106781186547,0.707106781186548,-8.65956056235493E-17));
#5859=DIRECTION('center_axis',(0.,-1.,0.));
#5860=DIRECTION('ref_axis',(0.,0.,-1.));
#5861=DIRECTION('center_axis',(0.866025403784439,0.,-0.5));
#5862=DIRECTION('ref_axis',(0.5,0.,0.866025403784439));
#5863=DIRECTION('',(-0.5,0.,-0.866025403784439));
#5864=DIRECTION('',(0.,-1.,0.));
#5865=DIRECTION('',(0.5,0.,0.866025403784439));
#5866=DIRECTION('',(0.,-1.,0.));
#5867=DIRECTION('center_axis',(1.60246890531964E-16,0.,-1.));
#5868=DIRECTION('ref_axis',(1.,0.,1.60246890531964E-16));
#5869=DIRECTION('',(-1.,0.,-1.60246890531964E-16));
#5870=DIRECTION('',(0.,-1.,0.));
#5871=DIRECTION('',(1.,0.,1.60246890531964E-16));
#5872=DIRECTION('center_axis',(-0.866025403784439,0.,-0.5));
#5873=DIRECTION('ref_axis',(0.5,0.,-0.866025403784439));
#5874=DIRECTION('',(-0.5,0.,0.866025403784439));
#5875=DIRECTION('',(0.,-1.,0.));
#5876=DIRECTION('',(0.5,0.,-0.866025403784439));
#5877=DIRECTION('center_axis',(-0.866025403784439,0.,0.5));
#5878=DIRECTION('ref_axis',(-0.5,0.,-0.866025403784439));
#5879=DIRECTION('',(0.5,0.,0.866025403784439));
#5880=DIRECTION('',(0.,-1.,0.));
#5881=DIRECTION('',(-0.5,0.,-0.866025403784439));
#5882=DIRECTION('center_axis',(-1.60246890531964E-16,0.,1.));
#5883=DIRECTION('ref_axis',(-1.,0.,-1.60246890531964E-16));
#5884=DIRECTION('',(1.,0.,1.60246890531964E-16));
#5885=DIRECTION('',(0.,-1.,0.));
#5886=DIRECTION('',(-1.,0.,-1.60246890531964E-16));
#5887=DIRECTION('center_axis',(0.866025403784439,0.,0.5));
#5888=DIRECTION('ref_axis',(-0.5,0.,0.866025403784439));
#5889=DIRECTION('',(0.5,0.,-0.866025403784439));
#5890=DIRECTION('',(-0.5,0.,0.866025403784439));
#5891=DIRECTION('center_axis',(0.,1.,0.));
#5892=DIRECTION('ref_axis',(1.,0.,0.));
#5893=DIRECTION('center_axis',(0.,-1.,0.));
#5894=DIRECTION('ref_axis',(0.,0.,-1.));
#7377=CARTESIAN_POINT('',(0.,0.,0.));
#7378=CARTESIAN_POINT('Origin',(0.3,0.4,0.));
#7379=CARTESIAN_POINT('',(-0.3,0.4,-3.67394039744206E-17));
#7380=CARTESIAN_POINT('Origin',(0.,0.4,0.));
#7381=CARTESIAN_POINT('Origin',(0.,0.375,0.));
#7382=CARTESIAN_POINT('',(-0.35,0.35,-4.28626379701573E-17));
#7383=CARTESIAN_POINT('Origin',(0.,0.35,0.));
#7384=CARTESIAN_POINT('',(-0.325,0.375,-3.9801020972289E-17));
#7385=CARTESIAN_POINT('Origin',(0.,0.19,0.));
#7386=CARTESIAN_POINT('',(-0.35,0.03,-4.28626379701574E-17));
#7387=CARTESIAN_POINT('Origin',(0.,0.03,0.));
#7388=CARTESIAN_POINT('',(-0.35,0.19,-4.28626379701574E-17));
#7389=CARTESIAN_POINT('Origin',(0.,0.0149999999999999,0.));
#7390=CARTESIAN_POINT('',(-0.32,-3.29597460435593E-17,-3.91886975727153E-17));
#7391=CARTESIAN_POINT('Origin',(0.,0.,0.));
#7392=CARTESIAN_POINT('',(-0.335,0.0149999999999999,-4.10256677714363E-17));
#7393=CARTESIAN_POINT('Origin',(0.22,0.,0.));
#7394=CARTESIAN_POINT('',(-0.22,-6.93889390390723E-18,-2.69422295812418E-17));
#7395=CARTESIAN_POINT('Origin',(0.,0.,0.));
#7396=CARTESIAN_POINT('Origin',(0.,-0.02,0.));
#7397=CARTESIAN_POINT('',(-0.1954,-0.0492,2.39295984553393E-17));
#7398=CARTESIAN_POINT('Origin',(0.,-0.0492,0.));
#7399=CARTESIAN_POINT('',(-0.21,-0.02,-2.57175827820944E-17));
#7400=CARTESIAN_POINT('Origin',(0.,-0.8,0.));
#7401=CARTESIAN_POINT('',(-0.1954,-1.5646,2.39295984553393E-17));
#7402=CARTESIAN_POINT('Origin',(0.,-1.5646,0.));
#7403=CARTESIAN_POINT('',(-0.1954,-0.8,-2.39295984553393E-17));
#7404=CARTESIAN_POINT('Origin',(0.,-1.58,0.));
#7405=CARTESIAN_POINT('',(-0.16,-1.6,-1.95943487863577E-17));
#7406=CARTESIAN_POINT('Origin',(0.,-1.6,0.));
#7407=CARTESIAN_POINT('',(-0.18,-1.58,-2.20436423846524E-17));
#7408=CARTESIAN_POINT('Origin',(0.,-1.6,0.));
#7409=CARTESIAN_POINT('Origin',(0.0866025403784439,-0.4,-0.15));
#7410=CARTESIAN_POINT('',(0.173205080756888,-0.4,0.));
#7411=CARTESIAN_POINT('',(0.0866025403784439,-0.4,-0.15));
#7412=CARTESIAN_POINT('',(0.173205080756888,-0.4,0.));
#7413=CARTESIAN_POINT('',(0.0866025403784439,-0.64,-0.15));
#7414=CARTESIAN_POINT('',(0.0866025403784439,-0.4,-0.15));
#7415=CARTESIAN_POINT('',(0.173205080756888,-0.64,0.));
#7416=CARTESIAN_POINT('',(0.173205080756888,-0.64,0.));
#7417=CARTESIAN_POINT('',(0.173205080756888,-0.4,0.));
#7418=CARTESIAN_POINT('Origin',(-0.0866025403784438,-0.4,-0.15));
#7419=CARTESIAN_POINT('',(-0.0866025403784438,-0.4,-0.15));
#7420=CARTESIAN_POINT('',(0.0866025403784439,-0.4,-0.15));
#7421=CARTESIAN_POINT('',(-0.0866025403784438,-0.64,-0.15));
#7422=CARTESIAN_POINT('',(-0.0866025403784438,-0.4,-0.15));
#7423=CARTESIAN_POINT('',(0.0866025403784439,-0.64,-0.15));
#7424=CARTESIAN_POINT('Origin',(-0.173205080756888,-0.4,-2.77555756156289E-17));
#7425=CARTESIAN_POINT('',(-0.173205080756888,-0.4,-2.12115047744981E-17));
#7426=CARTESIAN_POINT('',(-0.0866025403784438,-0.4,-0.15));
#7427=CARTESIAN_POINT('',(-0.173205080756888,-0.64,-2.77555756156289E-17));
#7428=CARTESIAN_POINT('',(-0.173205080756888,-0.4,-2.12115047744981E-17));
#7429=CARTESIAN_POINT('',(-0.0866025403784438,-0.64,-0.15));
#7430=CARTESIAN_POINT('Origin',(-0.0866025403784439,-0.4,0.15));
#7431=CARTESIAN_POINT('',(-0.0866025403784439,-0.4,0.15));
#7432=CARTESIAN_POINT('',(-0.173205080756888,-0.4,-2.12115047744981E-17));
#7433=CARTESIAN_POINT('',(-0.0866025403784439,-0.64,0.15));
#7434=CARTESIAN_POINT('',(-0.0866025403784439,-0.4,0.15));
#7435=CARTESIAN_POINT('',(-0.173205080756888,-0.64,-2.12115047744981E-17));
#7436=CARTESIAN_POINT('Origin',(0.0866025403784439,-0.4,0.15));
#7437=CARTESIAN_POINT('',(0.0866025403784439,-0.4,0.15));
#7438=CARTESIAN_POINT('',(-0.0866025403784439,-0.4,0.15));
#7439=CARTESIAN_POINT('',(0.0866025403784439,-0.64,0.15));
#7440=CARTESIAN_POINT('',(0.0866025403784439,-0.4,0.15));
#7441=CARTESIAN_POINT('',(-0.0866025403784439,-0.64,0.15));
#7442=CARTESIAN_POINT('Origin',(0.173205080756888,-0.4,0.));
#7443=CARTESIAN_POINT('',(0.0866025403784439,-0.4,0.15));
#7444=CARTESIAN_POINT('',(0.0866025403784439,-0.64,0.15));
#7445=CARTESIAN_POINT('Origin',(0.,-0.4,-2.77555756156289E-17));
#7446=CARTESIAN_POINT('Origin',(0.,-0.64,-2.77555756156289E-17));
#7848=UNCERTAINTY_MEASURE_WITH_UNIT(LENGTH_MEASURE(0.001),#7898,
'DISTANCE_ACCURACY_VALUE',
'Maximum model space distance between geometric entities at asserted c
onnectivities');
#7865=UNCERTAINTY_MEASURE_WITH_UNIT(LENGTH_MEASURE(0.001),#7898,
'DISTANCE_ACCURACY_VALUE',
'Maximum model space distance between geometric entities at asserted c
onnectivities');
#7880=(
GEOMETRIC_REPRESENTATION_CONTEXT(3)
GLOBAL_UNCERTAINTY_ASSIGNED_CONTEXT((#7848))
GLOBAL_UNIT_ASSIGNED_CONTEXT((#7898,#7900,#7901))
REPRESENTATION_CONTEXT('','3D')
);
#7897=(
GEOMETRIC_REPRESENTATION_CONTEXT(3)
GLOBAL_UNCERTAINTY_ASSIGNED_CONTEXT((#7865))
GLOBAL_UNIT_ASSIGNED_CONTEXT((#7898,#7900,#7901))
REPRESENTATION_CONTEXT('','3D')
);
#7898=(
LENGTH_UNIT()
NAMED_UNIT(*)
SI_UNIT(.CENTI.,.METRE.)
);
#7900=(
NAMED_UNIT(*)
PLANE_ANGLE_UNIT()
SI_UNIT($,.RADIAN.)
);
#7901=(
NAMED_UNIT(*)
SI_UNIT($,.STERADIAN.)
SOLID_ANGLE_UNIT()
);
#7916=SHAPE_DEFINITION_REPRESENTATION(#7947,#8013);
#7947=PRODUCT_DEFINITION_SHAPE('',$,#8045);
#8013=SHAPE_REPRESENTATION('',(#4834),#7880);
#8030=PRODUCT_DEFINITION_CONTEXT('part definition',#8125,'design');
#8045=PRODUCT_DEFINITION('Cap Screw - M4x16','Cap Screw - M4x16',#8076,
#8030);
#8076=PRODUCT_DEFINITION_FORMATION('',$,#8141);
#8125=APPLICATION_CONTEXT(
'Core Data for Automotive Mechanical Design Process');
#8126=PRODUCT_CONTEXT('part definition',#8125,'mechanical');
#8141=PRODUCT('Cap Screw - M4x16','Cap Screw - M4x16',
'Cap Screw - M4x16',(#8126));
#8221=COLOUR_RGB('Black',0.12,0.14,0.17);
#8222=FILL_AREA_STYLE_COLOUR('',#8221);
#8223=FILL_AREA_STYLE('',(#8222));
#8224=SURFACE_STYLE_FILL_AREA(#8223);
#8225=SURFACE_SIDE_STYLE('',(#8224));
#8226=SURFACE_STYLE_USAGE(.BOTH.,#8225);
#8227=PRESENTATION_STYLE_ASSIGNMENT((#8226));
ENDSEC;
END-ISO-10303-21;
